ISO-10303-21;
HEADER;
/* Generated by software containing ST-Developer
 * from STEP Tools, Inc. (www.steptools.com) 
 */

FILE_DESCRIPTION(
/* description */ ('Independent equipment support assembly with bolted 600 x 500 mm welde
d perimeter frame, four adjustable legs and swivel feet. Nominal overa
ll height 518 mm. No load rating assigned.'),
/* implementation_level */ '2;1');

FILE_NAME(
/* name */ 'Flat washer M8.step',
/* time_stamp */ '2026-11-07T17:30:39-08:00',
/* author */ (''),
/* organization */ (''),
/* preprocessor_version */ 'ST-DEVELOPER v20.2',
/* originating_system */ 'Autodesk Translation Framework v15.17.0.0',
/* authorisation */ '');

FILE_SCHEMA (('AUTOMOTIVE_DESIGN { 1 0 10303 214 3 1 1 }'));
ENDSEC;

DATA;
#10=MECHANICAL_DESIGN_GEOMETRIC_PRESENTATION_REPRESENTATION('',(#2212),#63755);
#308=CIRCLE('',#14693,4.5);
#309=CIRCLE('',#14694,4.5);
#310=CIRCLE('',#14696,9.);
#311=CIRCLE('',#14697,9.);
#1713=CYLINDRICAL_SURFACE('',#14692,4.5);
#1714=CYLINDRICAL_SURFACE('',#14695,9.);
#2180=SHAPE_REPRESENTATION_RELATIONSHIP('SRR','None',#63864,#2196);
#2196=ADVANCED_BREP_SHAPE_REPRESENTATION('',(#2228),#63742);
#2212=STYLED_ITEM('',(#63961),#2228);
#2228=MANIFOLD_SOLID_BREP('Body1',#14313);
#2254=FACE_BOUND('',#3250,.T.);
#2255=FACE_BOUND('',#3252,.T.);
#2473=FACE_OUTER_BOUND('',#3247,.T.);
#2474=FACE_OUTER_BOUND('',#3248,.T.);
#2475=FACE_OUTER_BOUND('',#3249,.T.);
#2476=FACE_OUTER_BOUND('',#3251,.T.);
#3247=EDGE_LOOP('',(#10087,#10088,#10089,#10090));
#3248=EDGE_LOOP('',(#10091,#10092,#10093,#10094));
#3249=EDGE_LOOP('',(#10095));
#3250=EDGE_LOOP('',(#10096));
#3251=EDGE_LOOP('',(#10097));
#3252=EDGE_LOOP('',(#10098));
#4078=LINE('',#27989,#4914);
#4079=LINE('',#27995,#4915);
#4914=VECTOR('',#16091,4.5);
#4915=VECTOR('',#16098,9.);
#5878=VERTEX_POINT('',#27986);
#5879=VERTEX_POINT('',#27988);
#5880=VERTEX_POINT('',#27992);
#5881=VERTEX_POINT('',#27994);
#7466=EDGE_CURVE('',#5878,#5878,#308,.T.);
#7467=EDGE_CURVE('',#5878,#5879,#4078,.T.);
#7468=EDGE_CURVE('',#5879,#5879,#309,.T.);
#7469=EDGE_CURVE('',#5880,#5880,#310,.T.);
#7470=EDGE_CURVE('',#5880,#5881,#4079,.T.);
#7471=EDGE_CURVE('',#5881,#5881,#311,.T.);
#10087=ORIENTED_EDGE('',*,*,#7466,.F.);
#10088=ORIENTED_EDGE('',*,*,#7467,.T.);
#10089=ORIENTED_EDGE('',*,*,#7468,.T.);
#10090=ORIENTED_EDGE('',*,*,#7467,.F.);
#10091=ORIENTED_EDGE('',*,*,#7469,.F.);
#10092=ORIENTED_EDGE('',*,*,#7470,.T.);
#10093=ORIENTED_EDGE('',*,*,#7471,.T.);
#10094=ORIENTED_EDGE('',*,*,#7470,.F.);
#10095=ORIENTED_EDGE('',*,*,#7469,.T.);
#10096=ORIENTED_EDGE('',*,*,#7466,.T.);
#10097=ORIENTED_EDGE('',*,*,#7471,.F.);
#10098=ORIENTED_EDGE('',*,*,#7468,.F.);
#13445=PLANE('',#14698);
#13446=PLANE('',#14699);
#13719=ADVANCED_FACE('',(#2473),#1713,.F.);
#13720=ADVANCED_FACE('',(#2474),#1714,.T.);
#13721=ADVANCED_FACE('',(#2475,#2254),#13445,.T.);
#13722=ADVANCED_FACE('',(#2476,#2255),#13446,.F.);
#14313=CLOSED_SHELL('',(#13719,#13720,#13721,#13722));
#14691=AXIS2_PLACEMENT_3D('',#27984,#16085,#16086);
#14692=AXIS2_PLACEMENT_3D('',#27985,#16087,#16088);
#14693=AXIS2_PLACEMENT_3D('',#27987,#16089,#16090);
#14694=AXIS2_PLACEMENT_3D('',#27990,#16092,#16093);
#14695=AXIS2_PLACEMENT_3D('',#27991,#16094,#16095);
#14696=AXIS2_PLACEMENT_3D('',#27993,#16096,#16097);
#14697=AXIS2_PLACEMENT_3D('',#27996,#16099,#16100);
#14698=AXIS2_PLACEMENT_3D('',#27997,#16101,#16102);
#14699=AXIS2_PLACEMENT_3D('',#27998,#16103,#16104);
#16085=DIRECTION('axis',(0.,0.,1.));
#16086=DIRECTION('refdir',(1.,0.,0.));
#16087=DIRECTION('center_axis',(0.,0.,1.));
#16088=DIRECTION('ref_axis',(1.,0.,0.));
#16089=DIRECTION('center_axis',(0.,0.,-1.));
#16090=DIRECTION('ref_axis',(1.,0.,0.));
#16091=DIRECTION('',(0.,0.,-1.));
#16092=DIRECTION('center_axis',(0.,0.,-1.));
#16093=DIRECTION('ref_axis',(1.,0.,0.));
#16094=DIRECTION('center_axis',(0.,0.,1.));
#16095=DIRECTION('ref_axis',(1.,0.,0.));
#16096=DIRECTION('center_axis',(0.,0.,1.));
#16097=DIRECTION('ref_axis',(1.,0.,0.));
#16098=DIRECTION('',(0.,0.,-1.));
#16099=DIRECTION('center_axis',(0.,0.,1.));
#16100=DIRECTION('ref_axis',(1.,0.,0.));
#16101=DIRECTION('center_axis',(0.,0.,1.));
#16102=DIRECTION('ref_axis',(1.,0.,0.));
#16103=DIRECTION('center_axis',(0.,0.,1.));
#16104=DIRECTION('ref_axis',(1.,0.,0.));
#27984=CARTESIAN_POINT('',(0.,0.,0.));
#27985=CARTESIAN_POINT('Origin',(0.,0.,0.));
#27986=CARTESIAN_POINT('',(-4.5,-5.51091059616309E-16,2.));
#27987=CARTESIAN_POINT('Origin',(0.,0.,2.));
#27988=CARTESIAN_POINT('',(-4.5,-5.51091059616309E-16,0.));
#27989=CARTESIAN_POINT('',(-4.5,-5.51091059616309E-16,0.));
#27990=CARTESIAN_POINT('Origin',(0.,0.,0.));
#27991=CARTESIAN_POINT('Origin',(0.,0.,0.));
#27992=CARTESIAN_POINT('',(-9.,-1.10218211923262E-15,2.));
#27993=CARTESIAN_POINT('Origin',(0.,0.,2.));
#27994=CARTESIAN_POINT('',(-9.,-1.10218211923262E-15,0.));
#27995=CARTESIAN_POINT('',(-9.,-1.10218211923262E-15,0.));
#27996=CARTESIAN_POINT('Origin',(0.,0.,0.));
#27997=CARTESIAN_POINT('Origin',(0.,0.,2.));
#27998=CARTESIAN_POINT('Origin',(0.,0.,0.));
#63722=UNCERTAINTY_MEASURE_WITH_UNIT(LENGTH_MEASURE(0.01),#63756,
'DISTANCE_ACCURACY_VALUE',
'Maximum model space distance between geometric entities at asserted c
onnectivities');
#63735=UNCERTAINTY_MEASURE_WITH_UNIT(LENGTH_MEASURE(0.01),#63756,
'DISTANCE_ACCURACY_VALUE',
'Maximum model space distance between geometric entities at asserted c
onnectivities');
#63742=(
GEOMETRIC_REPRESENTATION_CONTEXT(3)
GLOBAL_UNCERTAINTY_ASSIGNED_CONTEXT((#63722))
GLOBAL_UNIT_ASSIGNED_CONTEXT((#63756,#63758,#63759))
REPRESENTATION_CONTEXT('','3D')
);
#63755=(
GEOMETRIC_REPRESENTATION_CONTEXT(3)
GLOBAL_UNCERTAINTY_ASSIGNED_CONTEXT((#63735))
GLOBAL_UNIT_ASSIGNED_CONTEXT((#63756,#63758,#63759))
REPRESENTATION_CONTEXT('','3D')
);
#63756=(
LENGTH_UNIT()
NAMED_UNIT(*)
SI_UNIT(.MILLI.,.METRE.)
);
#63758=(
NAMED_UNIT(*)
PLANE_ANGLE_UNIT()
SI_UNIT($,.RADIAN.)
);
#63759=(
NAMED_UNIT(*)
SI_UNIT($,.STERADIAN.)
SOLID_ANGLE_UNIT()
);
#63766=SHAPE_DEFINITION_REPRESENTATION(#63785,#63864);
#63785=PRODUCT_DEFINITION_SHAPE('',$,#63884);
#63864=SHAPE_REPRESENTATION('',(#14691),#63742);
#63877=PRODUCT_DEFINITION_CONTEXT('part definition',#63936,'design');
#63884=PRODUCT_DEFINITION('Flat Washer M8','Flat washer M8',#63903,#63877);
#63903=PRODUCT_DEFINITION_FORMATION('',$,#63944);
#63936=APPLICATION_CONTEXT(
'Core Data for Automotive Mechanical Design Process');
#63937=PRODUCT_CONTEXT('part definition',#63936,'mechanical');
#63944=PRODUCT('Flat Washer M8','Flat washer M8','NOT SPECIFIED',(#63937));
#63961=PRESENTATION_STYLE_ASSIGNMENT((#63968));
#63968=SURFACE_STYLE_USAGE(.BOTH.,#63975);
#63975=SURFACE_SIDE_STYLE('',(#63982));
#63982=SURFACE_STYLE_FILL_AREA(#63989);
#63989=FILL_AREA_STYLE('Light gray',(#63996));
#63996=FILL_AREA_STYLE_COLOUR('Light gray',#64003);
#64003=COLOUR_RGB('Light gray',0.725490196078431,0.752941176470588,0.792156862745098);
ENDSEC;
END-ISO-10303-21;
